ISO-10303-21;
HEADER;
/* Generated by software containing ST-Developer
 * from STEP Tools, Inc. (www.steptools.com) 
 */

FILE_DESCRIPTION(
/* description */ ('Ball-race swivel caster'),
/* implementation_level */ '2;1');

FILE_NAME(
/* name */ 'Hex Nut - M8.step',
/* time_stamp */ '2026-10-29T16:15:51-07:00',
/* author */ (''),
/* organization */ (''),
/* preprocessor_version */ 'ST-DEVELOPER v20.2',
/* originating_system */ 'Autodesk Translation Framework v15.17.0.0',
/* authorisation */ '');

FILE_SCHEMA (('AUTOMOTIVE_DESIGN { 1 0 10303 214 3 1 1 }'));
ENDSEC;

DATA;
#10=MECHANICAL_DESIGN_GEOMETRIC_PRESENTATION_REPRESENTATION('',(#313),#7816);
#13=(
BOUNDED_CURVE()
B_SPLINE_CURVE(2,(#6859,#6860,#6861),.UNSPECIFIED.,.F.,.F.)
B_SPLINE_CURVE_WITH_KNOTS((3,3),(0.14973948338295,0.97160236658079),
 .UNSPECIFIED.)
CURVE()
GEOMETRIC_REPRESENTATION_ITEM()
RATIONAL_B_SPLINE_CURVE((1.07140024848292,1.23714644374248,1.07140024848292))
REPRESENTATION_ITEM('')
);
#14=(
BOUNDED_CURVE()
B_SPLINE_CURVE(2,(#6863,#6864,#6865),.UNSPECIFIED.,.F.,.F.)
B_SPLINE_CURVE_WITH_KNOTS((3,3),(0.14973948338295,0.971602366580789),
 .UNSPECIFIED.)
CURVE()
GEOMETRIC_REPRESENTATION_ITEM()
RATIONAL_B_SPLINE_CURVE((1.07140024848292,1.23714644374248,1.07140024848292))
REPRESENTATION_ITEM('')
);
#15=(
BOUNDED_CURVE()
B_SPLINE_CURVE(2,(#6870,#6871,#6872),.UNSPECIFIED.,.F.,.F.)
B_SPLINE_CURVE_WITH_KNOTS((3,3),(0.14973948338295,0.97160236658079),
 .UNSPECIFIED.)
CURVE()
GEOMETRIC_REPRESENTATION_ITEM()
RATIONAL_B_SPLINE_CURVE((1.07140024848292,1.23714644374248,1.07140024848292))
REPRESENTATION_ITEM('')
);
#16=(
BOUNDED_CURVE()
B_SPLINE_CURVE(2,(#6874,#6875,#6876),.UNSPECIFIED.,.F.,.F.)
B_SPLINE_CURVE_WITH_KNOTS((3,3),(0.14973948338295,0.97160236658079),
 .UNSPECIFIED.)
CURVE()
GEOMETRIC_REPRESENTATION_ITEM()
RATIONAL_B_SPLINE_CURVE((1.07140024848292,1.23714644374248,1.07140024848292))
REPRESENTATION_ITEM('')
);
#17=(
BOUNDED_CURVE()
B_SPLINE_CURVE(2,(#6878,#6879,#6880),.UNSPECIFIED.,.F.,.F.)
B_SPLINE_CURVE_WITH_KNOTS((3,3),(0.14973948338295,0.971602366580789),
 .UNSPECIFIED.)
CURVE()
GEOMETRIC_REPRESENTATION_ITEM()
RATIONAL_B_SPLINE_CURVE((1.07140024848292,1.23714644374248,1.07140024848292))
REPRESENTATION_ITEM('')
);
#18=(
BOUNDED_CURVE()
B_SPLINE_CURVE(2,(#6881,#6882,#6883),.UNSPECIFIED.,.F.,.F.)
B_SPLINE_CURVE_WITH_KNOTS((3,3),(0.14973948338295,0.97160236658079),
 .UNSPECIFIED.)
CURVE()
GEOMETRIC_REPRESENTATION_ITEM()
RATIONAL_B_SPLINE_CURVE((1.07140024848292,1.23714644374248,1.07140024848292))
REPRESENTATION_ITEM('')
);
#19=(
BOUNDED_CURVE()
B_SPLINE_CURVE(2,(#6890,#6891,#6892),.UNSPECIFIED.,.F.,.F.)
B_SPLINE_CURVE_WITH_KNOTS((3,3),(0.14973948338295,0.97160236658079),
 .UNSPECIFIED.)
CURVE()
GEOMETRIC_REPRESENTATION_ITEM()
RATIONAL_B_SPLINE_CURVE((1.07140024848292,1.23714644374248,1.07140024848292))
REPRESENTATION_ITEM('')
);
#20=(
BOUNDED_CURVE()
B_SPLINE_CURVE(2,(#6894,#6895,#6896),.UNSPECIFIED.,.F.,.F.)
B_SPLINE_CURVE_WITH_KNOTS((3,3),(0.14973948338295,0.97160236658079),
 .UNSPECIFIED.)
CURVE()
GEOMETRIC_REPRESENTATION_ITEM()
RATIONAL_B_SPLINE_CURVE((1.07140024848292,1.23714644374248,1.07140024848292))
REPRESENTATION_ITEM('')
);
#21=(
BOUNDED_CURVE()
B_SPLINE_CURVE(2,(#6898,#6899,#6900),.UNSPECIFIED.,.F.,.F.)
B_SPLINE_CURVE_WITH_KNOTS((3,3),(0.14973948338295,0.971602366580789),
 .UNSPECIFIED.)
CURVE()
GEOMETRIC_REPRESENTATION_ITEM()
RATIONAL_B_SPLINE_CURVE((1.07140024848292,1.23714644374248,1.07140024848292))
REPRESENTATION_ITEM('')
);
#22=(
BOUNDED_CURVE()
B_SPLINE_CURVE(2,(#6902,#6903,#6904),.UNSPECIFIED.,.F.,.F.)
B_SPLINE_CURVE_WITH_KNOTS((3,3),(0.14973948338295,0.97160236658079),
 .UNSPECIFIED.)
CURVE()
GEOMETRIC_REPRESENTATION_ITEM()
RATIONAL_B_SPLINE_CURVE((1.07140024848292,1.23714644374248,1.07140024848292))
REPRESENTATION_ITEM('')
);
#23=(
BOUNDED_CURVE()
B_SPLINE_CURVE(2,(#6906,#6907,#6908),.UNSPECIFIED.,.F.,.F.)
B_SPLINE_CURVE_WITH_KNOTS((3,3),(0.14973948338295,0.97160236658079),
 .UNSPECIFIED.)
CURVE()
GEOMETRIC_REPRESENTATION_ITEM()
RATIONAL_B_SPLINE_CURVE((1.07140024848292,1.23714644374248,1.07140024848292))
REPRESENTATION_ITEM('')
);
#24=(
BOUNDED_CURVE()
B_SPLINE_CURVE(2,(#6909,#6910,#6911),.UNSPECIFIED.,.F.,.F.)
B_SPLINE_CURVE_WITH_KNOTS((3,3),(0.14973948338295,0.971602366580789),
 .UNSPECIFIED.)
CURVE()
GEOMETRIC_REPRESENTATION_ITEM()
RATIONAL_B_SPLINE_CURVE((1.07140024848292,1.23714644374248,1.07140024848292))
REPRESENTATION_ITEM('')
);
#25=CONICAL_SURFACE('',#4207,0.734027674973257,1.0471975511966);
#26=CONICAL_SURFACE('',#4209,0.734027674973257,1.0471975511966);
#264=SHAPE_REPRESENTATION_RELATIONSHIP('SRR','None',#7910,#284);
#284=ADVANCED_BREP_SHAPE_REPRESENTATION('',(#349),#7799);
#313=STYLED_ITEM('',(#8104),#349);
#349=MANIFOLD_SOLID_BREP('Body1',#3719);
#410=FACE_BOUND('',#868,.T.);
#411=FACE_BOUND('',#870,.T.);
#457=PLANE('',#4211);
#458=PLANE('',#4212);
#459=PLANE('',#4213);
#460=PLANE('',#4217);
#461=PLANE('',#4218);
#462=PLANE('',#4219);
#463=PLANE('',#4220);
#464=PLANE('',#4221);
#608=FACE_OUTER_BOUND('',#858,.T.);
#609=FACE_OUTER_BOUND('',#859,.T.);
#610=FACE_OUTER_BOUND('',#860,.T.);
#611=FACE_OUTER_BOUND('',#861,.T.);
#612=FACE_OUTER_BOUND('',#862,.T.);
#613=FACE_OUTER_BOUND('',#863,.T.);
#614=FACE_OUTER_BOUND('',#864,.T.);
#615=FACE_OUTER_BOUND('',#865,.T.);
#616=FACE_OUTER_BOUND('',#866,.T.);
#617=FACE_OUTER_BOUND('',#867,.T.);
#618=FACE_OUTER_BOUND('',#869,.T.);
#858=EDGE_LOOP('',(#2927,#2928,#2929,#2930,#2931,#2932,#2933,#2934,#2935));
#859=EDGE_LOOP('',(#2936,#2937,#2938,#2939,#2940,#2941,#2942,#2943,#2944));
#860=EDGE_LOOP('',(#2945,#2946,#2947,#2948));
#861=EDGE_LOOP('',(#2949,#2950,#2951,#2952));
#862=EDGE_LOOP('',(#2953,#2954,#2955,#2956));
#863=EDGE_LOOP('',(#2957,#2958,#2959,#2960));
#864=EDGE_LOOP('',(#2961,#2962,#2963,#2964));
#865=EDGE_LOOP('',(#2965,#2966,#2967,#2968));
#866=EDGE_LOOP('',(#2969,#2970,#2971,#2972));
#867=EDGE_LOOP('',(#2973));
#868=EDGE_LOOP('',(#2974));
#869=EDGE_LOOP('',(#2975));
#870=EDGE_LOOP('',(#2976));
#1058=LINE('',#6867,#1213);
#1059=LINE('',#6888,#1214);
#1060=LINE('',#6913,#1215);
#1061=LINE('',#6914,#1216);
#1062=LINE('',#6916,#1217);
#1063=LINE('',#6918,#1218);
#1064=LINE('',#6923,#1219);
#1065=LINE('',#6926,#1220);
#1066=LINE('',#6928,#1221);
#1213=VECTOR('',#5028,0.734027674973257);
#1214=VECTOR('',#5035,0.734027674973257);
#1215=VECTOR('',#5038,1.);
#1216=VECTOR('',#5039,1.);
#1217=VECTOR('',#5042,1.);
#1218=VECTOR('',#5045,1.);
#1219=VECTOR('',#5050,0.4);
#1220=VECTOR('',#5055,1.);
#1221=VECTOR('',#5058,1.);
#1469=CIRCLE('',#4208,0.6175);
#1470=CIRCLE('',#4210,0.6175);
#1471=CIRCLE('',#4215,0.338975);
#1472=CIRCLE('',#4216,0.338975);
#1763=VERTEX_POINT('',#6857);
#1764=VERTEX_POINT('',#6858);
#1765=VERTEX_POINT('',#6862);
#1766=VERTEX_POINT('',#6866);
#1767=VERTEX_POINT('',#6869);
#1768=VERTEX_POINT('',#6873);
#1769=VERTEX_POINT('',#6877);
#1770=VERTEX_POINT('',#6885);
#1771=VERTEX_POINT('',#6887);
#1772=VERTEX_POINT('',#6889);
#1773=VERTEX_POINT('',#6893);
#1774=VERTEX_POINT('',#6897);
#1775=VERTEX_POINT('',#6901);
#1776=VERTEX_POINT('',#6905);
#1777=VERTEX_POINT('',#6920);
#1778=VERTEX_POINT('',#6922);
#2183=EDGE_CURVE('',#1763,#1764,#13,.T.);
#2184=EDGE_CURVE('',#1765,#1763,#14,.T.);
#2185=EDGE_CURVE('',#1765,#1766,#1058,.T.);
#2186=EDGE_CURVE('',#1766,#1766,#1469,.T.);
#2187=EDGE_CURVE('',#1767,#1765,#15,.T.);
#2188=EDGE_CURVE('',#1768,#1767,#16,.T.);
#2189=EDGE_CURVE('',#1769,#1768,#17,.T.);
#2190=EDGE_CURVE('',#1764,#1769,#18,.T.);
#2191=EDGE_CURVE('',#1770,#1770,#1470,.T.);
#2192=EDGE_CURVE('',#1770,#1771,#1059,.T.);
#2193=EDGE_CURVE('',#1772,#1771,#19,.T.);
#2194=EDGE_CURVE('',#1773,#1772,#20,.T.);
#2195=EDGE_CURVE('',#1774,#1773,#21,.T.);
#2196=EDGE_CURVE('',#1775,#1774,#22,.T.);
#2197=EDGE_CURVE('',#1776,#1775,#23,.T.);
#2198=EDGE_CURVE('',#1771,#1776,#24,.T.);
#2199=EDGE_CURVE('',#1767,#1776,#1060,.T.);
#2200=EDGE_CURVE('',#1768,#1775,#1061,.T.);
#2201=EDGE_CURVE('',#1765,#1771,#1062,.T.);
#2202=EDGE_CURVE('',#1763,#1772,#1063,.T.);
#2203=EDGE_CURVE('',#1777,#1777,#1471,.F.);
#2204=EDGE_CURVE('',#1777,#1778,#1064,.T.);
#2205=EDGE_CURVE('',#1778,#1778,#1472,.F.);
#2206=EDGE_CURVE('',#1764,#1773,#1065,.T.);
#2207=EDGE_CURVE('',#1769,#1774,#1066,.T.);
#2927=ORIENTED_EDGE('',*,*,#2183,.F.);
#2928=ORIENTED_EDGE('',*,*,#2184,.F.);
#2929=ORIENTED_EDGE('',*,*,#2185,.T.);
#2930=ORIENTED_EDGE('',*,*,#2186,.F.);
#2931=ORIENTED_EDGE('',*,*,#2185,.F.);
#2932=ORIENTED_EDGE('',*,*,#2187,.F.);
#2933=ORIENTED_EDGE('',*,*,#2188,.F.);
#2934=ORIENTED_EDGE('',*,*,#2189,.F.);
#2935=ORIENTED_EDGE('',*,*,#2190,.F.);
#2936=ORIENTED_EDGE('',*,*,#2191,.F.);
#2937=ORIENTED_EDGE('',*,*,#2192,.T.);
#2938=ORIENTED_EDGE('',*,*,#2193,.F.);
#2939=ORIENTED_EDGE('',*,*,#2194,.F.);
#2940=ORIENTED_EDGE('',*,*,#2195,.F.);
#2941=ORIENTED_EDGE('',*,*,#2196,.F.);
#2942=ORIENTED_EDGE('',*,*,#2197,.F.);
#2943=ORIENTED_EDGE('',*,*,#2198,.F.);
#2944=ORIENTED_EDGE('',*,*,#2192,.F.);
#2945=ORIENTED_EDGE('',*,*,#2188,.T.);
#2946=ORIENTED_EDGE('',*,*,#2199,.T.);
#2947=ORIENTED_EDGE('',*,*,#2197,.T.);
#2948=ORIENTED_EDGE('',*,*,#2200,.F.);
#2949=ORIENTED_EDGE('',*,*,#2187,.T.);
#2950=ORIENTED_EDGE('',*,*,#2201,.T.);
#2951=ORIENTED_EDGE('',*,*,#2198,.T.);
#2952=ORIENTED_EDGE('',*,*,#2199,.F.);
#2953=ORIENTED_EDGE('',*,*,#2184,.T.);
#2954=ORIENTED_EDGE('',*,*,#2202,.T.);
#2955=ORIENTED_EDGE('',*,*,#2193,.T.);
#2956=ORIENTED_EDGE('',*,*,#2201,.F.);
#2957=ORIENTED_EDGE('',*,*,#2203,.F.);
#2958=ORIENTED_EDGE('',*,*,#2204,.T.);
#2959=ORIENTED_EDGE('',*,*,#2205,.T.);
#2960=ORIENTED_EDGE('',*,*,#2204,.F.);
#2961=ORIENTED_EDGE('',*,*,#2183,.T.);
#2962=ORIENTED_EDGE('',*,*,#2206,.T.);
#2963=ORIENTED_EDGE('',*,*,#2194,.T.);
#2964=ORIENTED_EDGE('',*,*,#2202,.F.);
#2965=ORIENTED_EDGE('',*,*,#2189,.T.);
#2966=ORIENTED_EDGE('',*,*,#2200,.T.);
#2967=ORIENTED_EDGE('',*,*,#2196,.T.);
#2968=ORIENTED_EDGE('',*,*,#2207,.F.);
#2969=ORIENTED_EDGE('',*,*,#2190,.T.);
#2970=ORIENTED_EDGE('',*,*,#2207,.T.);
#2971=ORIENTED_EDGE('',*,*,#2195,.T.);
#2972=ORIENTED_EDGE('',*,*,#2206,.F.);
#2973=ORIENTED_EDGE('',*,*,#2191,.T.);
#2974=ORIENTED_EDGE('',*,*,#2203,.T.);
#2975=ORIENTED_EDGE('',*,*,#2186,.T.);
#2976=ORIENTED_EDGE('',*,*,#2205,.F.);
#3462=CYLINDRICAL_SURFACE('',#4214,0.338975);
#3579=ADVANCED_FACE('',(#608),#25,.T.);
#3580=ADVANCED_FACE('',(#609),#26,.T.);
#3581=ADVANCED_FACE('',(#610),#457,.T.);
#3582=ADVANCED_FACE('',(#611),#458,.T.);
#3583=ADVANCED_FACE('',(#612),#459,.T.);
#3584=ADVANCED_FACE('',(#613),#3462,.F.);
#3585=ADVANCED_FACE('',(#614),#460,.T.);
#3586=ADVANCED_FACE('',(#615),#461,.T.);
#3587=ADVANCED_FACE('',(#616),#462,.T.);
#3588=ADVANCED_FACE('',(#617,#410),#463,.T.);
#3589=ADVANCED_FACE('',(#618,#411),#464,.F.);
#3719=CLOSED_SHELL('',(#3579,#3580,#3581,#3582,#3583,#3584,#3585,#3586,
#3587,#3588,#3589));
#4206=AXIS2_PLACEMENT_3D('',#6855,#5024,#5025);
#4207=AXIS2_PLACEMENT_3D('',#6856,#5026,#5027);
#4208=AXIS2_PLACEMENT_3D('',#6868,#5029,#5030);
#4209=AXIS2_PLACEMENT_3D('',#6884,#5031,#5032);
#4210=AXIS2_PLACEMENT_3D('',#6886,#5033,#5034);
#4211=AXIS2_PLACEMENT_3D('',#6912,#5036,#5037);
#4212=AXIS2_PLACEMENT_3D('',#6915,#5040,#5041);
#4213=AXIS2_PLACEMENT_3D('',#6917,#5043,#5044);
#4214=AXIS2_PLACEMENT_3D('',#6919,#5046,#5047);
#4215=AXIS2_PLACEMENT_3D('',#6921,#5048,#5049);
#4216=AXIS2_PLACEMENT_3D('',#6924,#5051,#5052);
#4217=AXIS2_PLACEMENT_3D('',#6925,#5053,#5054);
#4218=AXIS2_PLACEMENT_3D('',#6927,#5056,#5057);
#4219=AXIS2_PLACEMENT_3D('',#6929,#5059,#5060);
#4220=AXIS2_PLACEMENT_3D('',#6930,#5061,#5062);
#4221=AXIS2_PLACEMENT_3D('',#6931,#5063,#5064);
#5024=DIRECTION('axis',(0.,0.,1.));
#5025=DIRECTION('refdir',(1.,0.,0.));
#5026=DIRECTION('center_axis',(0.,1.,0.));
#5027=DIRECTION('ref_axis',(1.,0.,0.));
#5028=DIRECTION('',(0.866025403784439,-0.5,1.06057523872491E-16));
#5029=DIRECTION('center_axis',(0.,-1.,0.));
#5030=DIRECTION('ref_axis',(1.,0.,0.));
#5031=DIRECTION('center_axis',(0.,-1.,0.));
#5032=DIRECTION('ref_axis',(1.,0.,0.));
#5033=DIRECTION('center_axis',(0.,1.,0.));
#5034=DIRECTION('ref_axis',(1.,0.,0.));
#5035=DIRECTION('',(-0.866025403784439,-0.5,-1.06057523872491E-16));
#5036=DIRECTION('center_axis',(1.4792020664489E-16,0.,-1.));
#5037=DIRECTION('ref_axis',(-1.,0.,-1.4792020664489E-16));
#5038=DIRECTION('',(0.,1.,0.));
#5039=DIRECTION('',(0.,1.,0.));
#5040=DIRECTION('center_axis',(-0.866025403784439,0.,-0.5));
#5041=DIRECTION('ref_axis',(-0.5,0.,0.866025403784439));
#5042=DIRECTION('',(0.,1.,0.));
#5043=DIRECTION('center_axis',(-0.866025403784439,0.,0.5));
#5044=DIRECTION('ref_axis',(0.5,0.,0.866025403784439));
#5045=DIRECTION('',(0.,1.,0.));
#5046=DIRECTION('center_axis',(0.,1.,0.));
#5047=DIRECTION('ref_axis',(1.,0.,0.));
#5048=DIRECTION('center_axis',(0.,1.,0.));
#5049=DIRECTION('ref_axis',(1.,0.,0.));
#5050=DIRECTION('',(0.,-1.,0.));
#5051=DIRECTION('center_axis',(0.,1.,0.));
#5052=DIRECTION('ref_axis',(1.,0.,0.));
#5053=DIRECTION('center_axis',(-2.95840413289779E-16,0.,1.));
#5054=DIRECTION('ref_axis',(1.,0.,2.95840413289779E-16));
#5055=DIRECTION('',(0.,1.,0.));
#5056=DIRECTION('center_axis',(0.866025403784439,0.,-0.5));
#5057=DIRECTION('ref_axis',(-0.5,0.,-0.866025403784439));
#5058=DIRECTION('',(0.,1.,0.));
#5059=DIRECTION('center_axis',(0.866025403784439,0.,0.5));
#5060=DIRECTION('ref_axis',(0.5,0.,-0.866025403784439));
#5061=DIRECTION('center_axis',(0.,1.,0.));
#5062=DIRECTION('ref_axis',(1.,0.,0.));
#5063=DIRECTION('center_axis',(0.,1.,0.));
#5064=DIRECTION('ref_axis',(1.,0.,0.));
#6855=CARTESIAN_POINT('',(0.,0.,0.));
#6856=CARTESIAN_POINT('Origin',(0.,0.067277284513851,0.));
#6857=CARTESIAN_POINT('',(-0.375277674973257,0.0768195421087395,0.65));
#6858=CARTESIAN_POINT('',(0.375277674973257,0.0768195421087395,0.65));
#6859=CARTESIAN_POINT('Ctrl Pts',(-0.375277674973257,0.0768195421087395,
0.65));
#6860=CARTESIAN_POINT('Ctrl Pts',(1.66533453693773E-13,-0.0315137912242439,
0.65));
#6861=CARTESIAN_POINT('Ctrl Pts',(0.375277674973257,0.0768195421087394,
0.65));
#6862=CARTESIAN_POINT('',(-0.750555349946514,0.0768195421087394,-9.19165206894919E-17));
#6863=CARTESIAN_POINT('Ctrl Pts',(-0.750555349946514,0.0768195421087394,
-9.19165206894919E-17));
#6864=CARTESIAN_POINT('Ctrl Pts',(-0.562916512459802,-0.0315137912242434,
0.325000000000144));
#6865=CARTESIAN_POINT('Ctrl Pts',(-0.375277674973257,0.0768195421087395,
0.65));
#6866=CARTESIAN_POINT('',(-0.6175,-2.77555756156289E-17,-7.5621939847349E-17));
#6867=CARTESIAN_POINT('',(-0.734027674973257,0.067277284513851,-8.98924642641573E-17));
#6868=CARTESIAN_POINT('Origin',(0.,0.,0.));
#6869=CARTESIAN_POINT('',(-0.375277674973257,0.0768195421087395,-0.65));
#6870=CARTESIAN_POINT('Ctrl Pts',(-0.375277674973257,0.0768195421087395,
-0.65));
#6871=CARTESIAN_POINT('Ctrl Pts',(-0.562916512459968,-0.0315137912242437,
-0.324999999999856));
#6872=CARTESIAN_POINT('Ctrl Pts',(-0.750555349946514,0.0768195421087395,
-9.19165206894919E-17));
#6873=CARTESIAN_POINT('',(0.375277674973257,0.0768195421087395,-0.65));
#6874=CARTESIAN_POINT('Ctrl Pts',(0.375277674973257,0.0768195421087395,
-0.65));
#6875=CARTESIAN_POINT('Ctrl Pts',(-1.66144875635155E-13,-0.0315137912242437,
-0.65));
#6876=CARTESIAN_POINT('Ctrl Pts',(-0.375277674973257,0.0768195421087395,
-0.65));
#6877=CARTESIAN_POINT('',(0.750555349946514,0.0768195421087394,0.));
#6878=CARTESIAN_POINT('Ctrl Pts',(0.750555349946514,0.0768195421087394,
0.));
#6879=CARTESIAN_POINT('Ctrl Pts',(0.562916512459802,-0.0315137912242436,
-0.325000000000144));
#6880=CARTESIAN_POINT('Ctrl Pts',(0.375277674973257,0.0768195421087395,
-0.65));
#6881=CARTESIAN_POINT('Ctrl Pts',(0.375277674973257,0.0768195421087394,
0.65));
#6882=CARTESIAN_POINT('Ctrl Pts',(0.562916512459968,-0.0315137912242439,
0.324999999999856));
#6883=CARTESIAN_POINT('Ctrl Pts',(0.750555349946514,0.0768195421087394,
0.));
#6884=CARTESIAN_POINT('Origin',(0.,0.612722715486149,0.));
#6885=CARTESIAN_POINT('',(-0.6175,0.68,-7.5621939847349E-17));
#6886=CARTESIAN_POINT('Origin',(0.,0.68,0.));
#6887=CARTESIAN_POINT('',(-0.750555349946514,0.603180457891261,-9.19165206894919E-17));
#6888=CARTESIAN_POINT('',(-0.734027674973257,0.612722715486149,-8.98924642641573E-17));
#6889=CARTESIAN_POINT('',(-0.375277674973257,0.603180457891261,0.65));
#6890=CARTESIAN_POINT('Ctrl Pts',(-0.375277674973257,0.603180457891261,
0.65));
#6891=CARTESIAN_POINT('Ctrl Pts',(-0.562916512459968,0.711513791224243,
0.324999999999856));
#6892=CARTESIAN_POINT('Ctrl Pts',(-0.750555349946514,0.603180457891261,
-9.19165206894919E-17));
#6893=CARTESIAN_POINT('',(0.375277674973257,0.603180457891261,0.65));
#6894=CARTESIAN_POINT('Ctrl Pts',(0.375277674973257,0.603180457891261,0.65));
#6895=CARTESIAN_POINT('Ctrl Pts',(-1.66755498298699E-13,0.711513791224244,
0.65));
#6896=CARTESIAN_POINT('Ctrl Pts',(-0.375277674973257,0.603180457891261,
0.65));
#6897=CARTESIAN_POINT('',(0.750555349946514,0.603180457891261,0.));
#6898=CARTESIAN_POINT('Ctrl Pts',(0.750555349946514,0.603180457891261,0.));
#6899=CARTESIAN_POINT('Ctrl Pts',(0.562916512459802,0.711513791224244,0.325000000000144));
#6900=CARTESIAN_POINT('Ctrl Pts',(0.375277674973257,0.603180457891261,0.65));
#6901=CARTESIAN_POINT('',(0.375277674973257,0.603180457891261,-0.65));
#6902=CARTESIAN_POINT('Ctrl Pts',(0.375277674973257,0.603180457891261,-0.65));
#6903=CARTESIAN_POINT('Ctrl Pts',(0.562916512459969,0.711513791224244,-0.324999999999856));
#6904=CARTESIAN_POINT('Ctrl Pts',(0.750555349946514,0.603180457891261,0.));
#6905=CARTESIAN_POINT('',(-0.375277674973257,0.603180457891261,-0.65));
#6906=CARTESIAN_POINT('Ctrl Pts',(-0.375277674973257,0.603180457891261,
-0.65));
#6907=CARTESIAN_POINT('Ctrl Pts',(1.66422431391311E-13,0.711513791224244,
-0.65));
#6908=CARTESIAN_POINT('Ctrl Pts',(0.375277674973257,0.603180457891261,-0.65));
#6909=CARTESIAN_POINT('Ctrl Pts',(-0.750555349946514,0.603180457891261,
-9.19165206894919E-17));
#6910=CARTESIAN_POINT('Ctrl Pts',(-0.562916512459802,0.711513791224244,
-0.325000000000144));
#6911=CARTESIAN_POINT('Ctrl Pts',(-0.375277674973257,0.603180457891261,
-0.65));
#6912=CARTESIAN_POINT('Origin',(0.375277674973257,0.,-0.65));
#6913=CARTESIAN_POINT('',(-0.375277674973257,0.,-0.65));
#6914=CARTESIAN_POINT('',(0.375277674973257,0.,-0.65));
#6915=CARTESIAN_POINT('Origin',(-0.375277674973257,0.,-0.65));
#6916=CARTESIAN_POINT('',(-0.750555349946514,0.,-9.19165206894919E-17));
#6917=CARTESIAN_POINT('Origin',(-0.750555349946514,0.,-9.19165206894919E-17));
#6918=CARTESIAN_POINT('',(-0.375277674973257,0.,0.65));
#6919=CARTESIAN_POINT('Origin',(0.,0.,0.));
#6920=CARTESIAN_POINT('',(-0.338975,0.68,4.15124648740974E-17));
#6921=CARTESIAN_POINT('Origin',(0.,0.68,0.));
#6922=CARTESIAN_POINT('',(-0.338975,0.,4.15124648740974E-17));
#6923=CARTESIAN_POINT('',(-0.338975,0.,4.15124648740974E-17));
#6924=CARTESIAN_POINT('Origin',(0.,0.,0.));
#6925=CARTESIAN_POINT('Origin',(-0.375277674973257,0.,0.65));
#6926=CARTESIAN_POINT('',(0.375277674973257,0.,0.65));
#6927=CARTESIAN_POINT('Origin',(0.750555349946514,0.,0.));
#6928=CARTESIAN_POINT('',(0.750555349946514,0.,0.));
#6929=CARTESIAN_POINT('Origin',(0.375277674973257,0.,0.65));
#6930=CARTESIAN_POINT('Origin',(0.,0.68,-1.11022302462516E-16));
#6931=CARTESIAN_POINT('Origin',(0.,0.,-1.11022302462516E-16));
#7772=UNCERTAINTY_MEASURE_WITH_UNIT(LENGTH_MEASURE(0.001),#7817,
'DISTANCE_ACCURACY_VALUE',
'Maximum model space distance between geometric entities at asserted c
onnectivities');
#7789=UNCERTAINTY_MEASURE_WITH_UNIT(LENGTH_MEASURE(0.001),#7817,
'DISTANCE_ACCURACY_VALUE',
'Maximum model space distance between geometric entities at asserted c
onnectivities');
#7799=(
GEOMETRIC_REPRESENTATION_CONTEXT(3)
GLOBAL_UNCERTAINTY_ASSIGNED_CONTEXT((#7772))
GLOBAL_UNIT_ASSIGNED_CONTEXT((#7817,#7819,#7820))
REPRESENTATION_CONTEXT('','3D')
);
#7816=(
GEOMETRIC_REPRESENTATION_CONTEXT(3)
GLOBAL_UNCERTAINTY_ASSIGNED_CONTEXT((#7789))
GLOBAL_UNIT_ASSIGNED_CONTEXT((#7817,#7819,#7820))
REPRESENTATION_CONTEXT('','3D')
);
#7817=(
LENGTH_UNIT()
NAMED_UNIT(*)
SI_UNIT(.CENTI.,.METRE.)
);
#7819=(
NAMED_UNIT(*)
PLANE_ANGLE_UNIT()
SI_UNIT($,.RADIAN.)
);
#7820=(
NAMED_UNIT(*)
SI_UNIT($,.STERADIAN.)
SOLID_ANGLE_UNIT()
);
#7830=SHAPE_DEFINITION_REPRESENTATION(#7859,#7910);
#7859=PRODUCT_DEFINITION_SHAPE('',$,#7937);
#7910=SHAPE_REPRESENTATION('',(#4206),#7799);
#7927=PRODUCT_DEFINITION_CONTEXT('part definition',#8007,'design');
#7937=PRODUCT_DEFINITION('Hex Nut - M8','Hex Nut - M8',#7963,#7927);
#7963=PRODUCT_DEFINITION_FORMATION('',$,#8018);
#8007=APPLICATION_CONTEXT(
'Core Data for Automotive Mechanical Design Process');
#8008=PRODUCT_CONTEXT('part definition',#8007,'mechanical');
#8018=PRODUCT('Hex Nut - M8','Hex Nut - M8','Hex Nut - M8',(#8008));
#8098=COLOUR_RGB('Black',0.12,0.14,0.17);
#8099=FILL_AREA_STYLE_COLOUR('',#8098);
#8100=FILL_AREA_STYLE('',(#8099));
#8101=SURFACE_STYLE_FILL_AREA(#8100);
#8102=SURFACE_SIDE_STYLE('',(#8101));
#8103=SURFACE_STYLE_USAGE(.BOTH.,#8102);
#8104=PRESENTATION_STYLE_ASSIGNMENT((#8103));
ENDSEC;
END-ISO-10303-21;
